ISO-10303-21;
HEADER;
/* Generated by software containing ST-Developer
 * from STEP Tools, Inc. (www.steptools.com) 
 */

FILE_DESCRIPTION(
/* description */ ('Hand-crank flanged shaft unit'),
/* implementation_level */ '2;1');

FILE_NAME(
/* name */ 'Flange bolt sleeve (1).step',
/* time_stamp */ '2026-10-27T18:35:45-07:00',
/* author */ (''),
/* organization */ (''),
/* preprocessor_version */ 'ST-DEVELOPER v20.2',
/* originating_system */ 'Autodesk Translation Framework v15.17.0.0',
/* authorisation */ '');

FILE_SCHEMA (('AUTOMOTIVE_DESIGN { 1 0 10303 214 3 1 1 }'));
ENDSEC;

DATA;
#10=MECHANICAL_DESIGN_GEOMETRIC_PRESENTATION_REPRESENTATION('',(#281),#6805);
#241=SHAPE_REPRESENTATION_RELATIONSHIP('SRR','None',#6902,#261);
#261=ADVANCED_BREP_SHAPE_REPRESENTATION('',(#302),#6785);
#281=STYLED_ITEM('',(#7098),#302);
#302=MANIFOLD_SOLID_BREP('Body1',#3322);
#344=FACE_BOUND('',#760,.T.);
#345=FACE_BOUND('',#762,.T.);
#428=PLANE('',#3617);
#429=PLANE('',#3618);
#545=FACE_OUTER_BOUND('',#757,.T.);
#546=FACE_OUTER_BOUND('',#758,.T.);
#547=FACE_OUTER_BOUND('',#759,.T.);
#548=FACE_OUTER_BOUND('',#761,.T.);
#757=EDGE_LOOP('',(#2395,#2396,#2397,#2398));
#758=EDGE_LOOP('',(#2399,#2400,#2401,#2402));
#759=EDGE_LOOP('',(#2403));
#760=EDGE_LOOP('',(#2404));
#761=EDGE_LOOP('',(#2405));
#762=EDGE_LOOP('',(#2406));
#1029=LINE('',#5091,#1257);
#1030=LINE('',#5097,#1258);
#1257=VECTOR('',#4106,0.425);
#1258=VECTOR('',#4113,0.595);
#1461=CIRCLE('',#3612,0.425);
#1462=CIRCLE('',#3613,0.425);
#1463=CIRCLE('',#3615,0.595);
#1464=CIRCLE('',#3616,0.595);
#1617=VERTEX_POINT('',#5088);
#1618=VERTEX_POINT('',#5090);
#1619=VERTEX_POINT('',#5094);
#1620=VERTEX_POINT('',#5096);
#1915=EDGE_CURVE('',#1617,#1617,#1461,.T.);
#1916=EDGE_CURVE('',#1617,#1618,#1029,.T.);
#1917=EDGE_CURVE('',#1618,#1618,#1462,.T.);
#1918=EDGE_CURVE('',#1619,#1619,#1463,.T.);
#1919=EDGE_CURVE('',#1619,#1620,#1030,.T.);
#1920=EDGE_CURVE('',#1620,#1620,#1464,.T.);
#2395=ORIENTED_EDGE('',*,*,#1915,.F.);
#2396=ORIENTED_EDGE('',*,*,#1916,.T.);
#2397=ORIENTED_EDGE('',*,*,#1917,.T.);
#2398=ORIENTED_EDGE('',*,*,#1916,.F.);
#2399=ORIENTED_EDGE('',*,*,#1918,.F.);
#2400=ORIENTED_EDGE('',*,*,#1919,.T.);
#2401=ORIENTED_EDGE('',*,*,#1920,.T.);
#2402=ORIENTED_EDGE('',*,*,#1919,.F.);
#2403=ORIENTED_EDGE('',*,*,#1918,.T.);
#2404=ORIENTED_EDGE('',*,*,#1915,.T.);
#2405=ORIENTED_EDGE('',*,*,#1920,.F.);
#2406=ORIENTED_EDGE('',*,*,#1917,.F.);
#3079=CYLINDRICAL_SURFACE('',#3611,0.425);
#3080=CYLINDRICAL_SURFACE('',#3614,0.595);
#3162=ADVANCED_FACE('',(#545),#3079,.F.);
#3163=ADVANCED_FACE('',(#546),#3080,.T.);
#3164=ADVANCED_FACE('',(#547,#344),#428,.T.);
#3165=ADVANCED_FACE('',(#548,#345),#429,.F.);
#3322=CLOSED_SHELL('',(#3162,#3163,#3164,#3165));
#3610=AXIS2_PLACEMENT_3D('',#5086,#4100,#4101);
#3611=AXIS2_PLACEMENT_3D('',#5087,#4102,#4103);
#3612=AXIS2_PLACEMENT_3D('',#5089,#4104,#4105);
#3613=AXIS2_PLACEMENT_3D('',#5092,#4107,#4108);
#3614=AXIS2_PLACEMENT_3D('',#5093,#4109,#4110);
#3615=AXIS2_PLACEMENT_3D('',#5095,#4111,#4112);
#3616=AXIS2_PLACEMENT_3D('',#5098,#4114,#4115);
#3617=AXIS2_PLACEMENT_3D('',#5099,#4116,#4117);
#3618=AXIS2_PLACEMENT_3D('',#5100,#4118,#4119);
#4100=DIRECTION('axis',(0.,0.,1.));
#4101=DIRECTION('refdir',(1.,0.,0.));
#4102=DIRECTION('center_axis',(0.,1.,0.));
#4103=DIRECTION('ref_axis',(1.,0.,0.));
#4104=DIRECTION('center_axis',(0.,-1.,0.));
#4105=DIRECTION('ref_axis',(1.,0.,0.));
#4106=DIRECTION('',(0.,-1.,0.));
#4107=DIRECTION('center_axis',(0.,-1.,0.));
#4108=DIRECTION('ref_axis',(1.,0.,0.));
#4109=DIRECTION('center_axis',(0.,1.,0.));
#4110=DIRECTION('ref_axis',(1.,0.,0.));
#4111=DIRECTION('center_axis',(0.,1.,0.));
#4112=DIRECTION('ref_axis',(1.,0.,0.));
#4113=DIRECTION('',(0.,-1.,0.));
#4114=DIRECTION('center_axis',(0.,1.,0.));
#4115=DIRECTION('ref_axis',(1.,0.,0.));
#4116=DIRECTION('center_axis',(0.,1.,0.));
#4117=DIRECTION('ref_axis',(1.,0.,0.));
#4118=DIRECTION('center_axis',(0.,1.,0.));
#4119=DIRECTION('ref_axis',(1.,0.,0.));
#5086=CARTESIAN_POINT('',(0.,0.,0.));
#5087=CARTESIAN_POINT('Origin',(-3.2,-1.,10.7));
#5088=CARTESIAN_POINT('',(-3.625,0.,10.7));
#5089=CARTESIAN_POINT('Origin',(-3.2,0.,10.7));
#5090=CARTESIAN_POINT('',(-3.625,-1.,10.7));
#5091=CARTESIAN_POINT('',(-3.625,-1.,10.7));
#5092=CARTESIAN_POINT('Origin',(-3.2,-1.,10.7));
#5093=CARTESIAN_POINT('Origin',(-3.2,-1.,10.7));
#5094=CARTESIAN_POINT('',(-3.795,0.,10.7));
#5095=CARTESIAN_POINT('Origin',(-3.2,0.,10.7));
#5096=CARTESIAN_POINT('',(-3.795,-1.,10.7));
#5097=CARTESIAN_POINT('',(-3.795,-1.,10.7));
#5098=CARTESIAN_POINT('Origin',(-3.2,-1.,10.7));
#5099=CARTESIAN_POINT('Origin',(-3.2,0.,10.7));
#5100=CARTESIAN_POINT('Origin',(-3.2,-1.,10.7));
#6760=UNCERTAINTY_MEASURE_WITH_UNIT(LENGTH_MEASURE(0.001),#6806,
'DISTANCE_ACCURACY_VALUE',
'Maximum model space distance between geometric entities at asserted c
onnectivities');
#6780=UNCERTAINTY_MEASURE_WITH_UNIT(LENGTH_MEASURE(0.001),#6806,
'DISTANCE_ACCURACY_VALUE',
'Maximum model space distance between geometric entities at asserted c
onnectivities');
#6785=(
GEOMETRIC_REPRESENTATION_CONTEXT(3)
GLOBAL_UNCERTAINTY_ASSIGNED_CONTEXT((#6760))
GLOBAL_UNIT_ASSIGNED_CONTEXT((#6806,#6808,#6809))
REPRESENTATION_CONTEXT('','3D')
);
#6805=(
GEOMETRIC_REPRESENTATION_CONTEXT(3)
GLOBAL_UNCERTAINTY_ASSIGNED_CONTEXT((#6780))
GLOBAL_UNIT_ASSIGNED_CONTEXT((#6806,#6808,#6809))
REPRESENTATION_CONTEXT('','3D')
);
#6806=(
LENGTH_UNIT()
NAMED_UNIT(*)
SI_UNIT(.CENTI.,.METRE.)
);
#6808=(
NAMED_UNIT(*)
PLANE_ANGLE_UNIT()
SI_UNIT($,.RADIAN.)
);
#6809=(
NAMED_UNIT(*)
SI_UNIT($,.STERADIAN.)
SOLID_ANGLE_UNIT()
);
#6814=SHAPE_DEFINITION_REPRESENTATION(#6838,#6902);
#6838=PRODUCT_DEFINITION_SHAPE('',$,#6927);
#6902=SHAPE_REPRESENTATION('',(#3610),#6785);
#6922=PRODUCT_DEFINITION_CONTEXT('part definition',#6996,'design');
#6927=PRODUCT_DEFINITION('Flange bolt sleeve (1)',
'Flange bolt sleeve (1)',#6951,#6922);
#6951=PRODUCT_DEFINITION_FORMATION('',$,#7002);
#6996=APPLICATION_CONTEXT(
'Core Data for Automotive Mechanical Design Process');
#6997=PRODUCT_CONTEXT('part definition',#6996,'mechanical');
#7002=PRODUCT('Flange bolt sleeve (1)','Flange bolt sleeve (1)',
'Flange bolt sleeve (1)',(#6997));
#7092=COLOUR_RGB('Black',0.12,0.14,0.17);
#7093=FILL_AREA_STYLE_COLOUR('',#7092);
#7094=FILL_AREA_STYLE('',(#7093));
#7095=SURFACE_STYLE_FILL_AREA(#7094);
#7096=SURFACE_SIDE_STYLE('',(#7095));
#7097=SURFACE_STYLE_USAGE(.BOTH.,#7096);
#7098=PRESENTATION_STYLE_ASSIGNMENT((#7097));
ENDSEC;
END-ISO-10303-21;
